ISO-10303-21;
HEADER;
/* Generated by software containing ST-Developer
 * from STEP Tools, Inc. (www.steptools.com) 
 */

FILE_DESCRIPTION(
/* description */ ('Timing belt drive module 2 mm Pitch Timing 20T-40T'),

/* implementation_level */ '2;1');

FILE_NAME(
/* name */ 'Input M3 set screw.step',
/* time_stamp */ '2026-10-28T03:25:12-07:00',
/* author */ (''),
/* organization */ (''),
/* preprocessor_version */ 'ST-DEVELOPER v20.2',
/* originating_system */ 'Autodesk Translation Framework v15.17.0.0',
/* authorisation */ '');

FILE_SCHEMA (('AUTOMOTIVE_DESIGN { 1 0 10303 214 3 1 1 }'));
ENDSEC;

DATA;
#10=MECHANICAL_DESIGN_GEOMETRIC_PRESENTATION_REPRESENTATION('',(#570),#17830);
#469=SHAPE_REPRESENTATION_RELATIONSHIP('SRR','None',#18042,#512);
#512=ADVANCED_BREP_SHAPE_REPRESENTATION('',(#626),#17817);
#570=STYLED_ITEM('',(#18324),#626);
#626=MANIFOLD_SOLID_BREP('Body1',#9029);
#920=PLANE('',#10241);
#921=PLANE('',#10242);
#1283=FACE_OUTER_BOUND('',#1906,.T.);
#1284=FACE_OUTER_BOUND('',#1907,.T.);
#1285=FACE_OUTER_BOUND('',#1908,.T.);
#1906=EDGE_LOOP('',(#7141,#7142,#7143,#7144));
#1907=EDGE_LOOP('',(#7145));
#1908=EDGE_LOOP('',(#7146));
#2494=CIRCLE('',#10239,0.15);
#2495=CIRCLE('',#10240,0.15);
#3088=LINE('',#16032,#3566);
#3566=VECTOR('',#12555,0.15);
#4217=VERTEX_POINT('',#16029);
#4218=VERTEX_POINT('',#16031);
#5253=EDGE_CURVE('',#4217,#4217,#2494,.T.);
#5254=EDGE_CURVE('',#4217,#4218,#3088,.T.);
#5255=EDGE_CURVE('',#4218,#4218,#2495,.T.);
#7141=ORIENTED_EDGE('',*,*,#5253,.F.);
#7142=ORIENTED_EDGE('',*,*,#5254,.T.);
#7143=ORIENTED_EDGE('',*,*,#5255,.T.);
#7144=ORIENTED_EDGE('',*,*,#5254,.F.);
#7145=ORIENTED_EDGE('',*,*,#5253,.T.);
#7146=ORIENTED_EDGE('',*,*,#5255,.F.);
#8306=CYLINDRICAL_SURFACE('',#10238,0.15);
#8781=ADVANCED_FACE('',(#1283),#8306,.T.);
#8782=ADVANCED_FACE('',(#1284),#920,.T.);
#8783=ADVANCED_FACE('',(#1285),#921,.F.);
#9029=CLOSED_SHELL('',(#8781,#8782,#8783));
#10237=AXIS2_PLACEMENT_3D('',#16027,#12549,#12550);
#10238=AXIS2_PLACEMENT_3D('',#16028,#12551,#12552);
#10239=AXIS2_PLACEMENT_3D('',#16030,#12553,#12554);
#10240=AXIS2_PLACEMENT_3D('',#16033,#12556,#12557);
#10241=AXIS2_PLACEMENT_3D('',#16034,#12558,#12559);
#10242=AXIS2_PLACEMENT_3D('',#16035,#12560,#12561);
#12549=DIRECTION('axis',(0.,0.,1.));
#12550=DIRECTION('refdir',(1.,0.,0.));
#12551=DIRECTION('center_axis',(0.,0.,1.));
#12552=DIRECTION('ref_axis',(1.,0.,0.));
#12553=DIRECTION('center_axis',(0.,0.,1.));
#12554=DIRECTION('ref_axis',(1.,0.,0.));
#12555=DIRECTION('',(0.,0.,-1.));
#12556=DIRECTION('center_axis',(0.,0.,1.));
#12557=DIRECTION('ref_axis',(1.,0.,0.));
#12558=DIRECTION('center_axis',(0.,0.,1.));
#12559=DIRECTION('ref_axis',(1.,0.,0.));
#12560=DIRECTION('center_axis',(0.,0.,1.));
#12561=DIRECTION('ref_axis',(1.,0.,0.));
#16027=CARTESIAN_POINT('',(0.,0.,0.));
#16028=CARTESIAN_POINT('Origin',(0.,-3.95,6.35));
#16029=CARTESIAN_POINT('',(-0.15,-3.95,6.6));
#16030=CARTESIAN_POINT('Origin',(0.,-3.95,6.6));
#16031=CARTESIAN_POINT('',(-0.15,-3.95,6.35));
#16032=CARTESIAN_POINT('',(-0.15,-3.95,6.35));
#16033=CARTESIAN_POINT('Origin',(0.,-3.95,6.35));
#16034=CARTESIAN_POINT('Origin',(0.,-3.95,6.6));
#16035=CARTESIAN_POINT('Origin',(0.,-3.95,6.35));
#17767=UNCERTAINTY_MEASURE_WITH_UNIT(LENGTH_MEASURE(0.001),#17831,
'DISTANCE_ACCURACY_VALUE',
'Maximum model space distance between geometric entities at asserted c
onnectivities');
#17780=UNCERTAINTY_MEASURE_WITH_UNIT(LENGTH_MEASURE(0.001),#17831,
'DISTANCE_ACCURACY_VALUE',
'Maximum model space distance between geometric entities at asserted c
onnectivities');
#17817=(
GEOMETRIC_REPRESENTATION_CONTEXT(3)
GLOBAL_UNCERTAINTY_ASSIGNED_CONTEXT((#17767))
GLOBAL_UNIT_ASSIGNED_CONTEXT((#17831,#17833,#17834))
REPRESENTATION_CONTEXT('','3D')
);
#17830=(
GEOMETRIC_REPRESENTATION_CONTEXT(3)
GLOBAL_UNCERTAINTY_ASSIGNED_CONTEXT((#17780))
GLOBAL_UNIT_ASSIGNED_CONTEXT((#17831,#17833,#17834))
REPRESENTATION_CONTEXT('','3D')
);
#17831=(
LENGTH_UNIT()
NAMED_UNIT(*)
SI_UNIT(.CENTI.,.METRE.)
);
#17833=(
NAMED_UNIT(*)
PLANE_ANGLE_UNIT()
SI_UNIT($,.RADIAN.)
);
#17834=(
NAMED_UNIT(*)
SI_UNIT($,.STERADIAN.)
SOLID_ANGLE_UNIT()
);
#17871=SHAPE_DEFINITION_REPRESENTATION(#17930,#18042);
#17930=PRODUCT_DEFINITION_SHAPE('',$,#18092);
#18042=SHAPE_REPRESENTATION('',(#10237),#17817);
#18055=PRODUCT_DEFINITION_CONTEXT('part definition',#18204,'design');
#18092=PRODUCT_DEFINITION('Input M3 set screw','Input M3 set screw',#18141,
#18055);
#18141=PRODUCT_DEFINITION_FORMATION('',$,#18242);
#18204=APPLICATION_CONTEXT(
'Core Data for Automotive Mechanical Design Process');
#18205=PRODUCT_CONTEXT('part definition',#18204,'mechanical');
#18242=PRODUCT('Input M3 set screw','Input M3 set screw',
'Input M3 set screw',(#18205));
#18318=COLOUR_RGB('Black',0.12,0.14,0.17);
#18319=FILL_AREA_STYLE_COLOUR('',#18318);
#18320=FILL_AREA_STYLE('',(#18319));
#18321=SURFACE_STYLE_FILL_AREA(#18320);
#18322=SURFACE_SIDE_STYLE('',(#18321));
#18323=SURFACE_STYLE_USAGE(.BOTH.,#18322);
#18324=PRESENTATION_STYLE_ASSIGNMENT((#18323));
ENDSEC;
END-ISO-10303-21;
